ISO-10303-21;
HEADER;
FILE_DESCRIPTION (('STEP AP214'),
    '1' );
FILE_NAME ('socket head cap screw_iso_ISO 4762 M10 x 80 - 32N.step',
    '2026-10-19T17:36:30',
    ( '' ),
    ( '' ),
    'SwSTEP 2.0',
    'SolidWorks 2025',
    '' );
FILE_SCHEMA (( 'AUTOMOTIVE_DESIGN' ));
ENDSEC;

DATA;
#12=ORIENTED_EDGE ( 'NONE', *, *, #10107, .F. ) ;
#17=FACE_OUTER_BOUND ( 'NONE', #5721, .T. ) ;
#56=CARTESIAN_POINT ( 'NONE',  ( 90.00000000000000000, 0.000000000000000000, 4.171999999999999709 ) ) ;
#74=CIRCLE ( 'NONE', #4934, 1.499999999999999556 ) ;
#85=AXIS2_PLACEMENT_3D ( 'NONE', #8229, #8169, #12160 ) ;
#89=ORIENTED_EDGE ( 'NONE', *, *, #5986, .F. ) ;
#106=ORIENTED_EDGE ( 'NONE', *, *, #5900, .F. ) ;
#112=AXIS2_PLACEMENT_3D ( 'NONE', #4795, #6504, #8414 ) ;
#115=FACE_OUTER_BOUND ( 'NONE', #4658, .T. ) ;
#119=CARTESIAN_POINT ( 'NONE',  ( 1.500000000000001332, 0.000000000000000000, 0.000000000000000000 ) ) ;
#145=EDGE_CURVE ( 'NONE', #6002, #9969, #12095, .T. ) ;
#147=DIRECTION ( 'NONE',  ( 0.000000000000000000, 0.000000000000000000, -1.000000000000000000 ) ) ;
#169=VERTEX_POINT ( 'NONE', #4475 ) ;
#207=DIRECTION ( 'NONE',  ( 1.000000000000000000, 0.000000000000000000, 0.000000000000000000 ) ) ;
#208=CARTESIAN_POINT ( 'NONE',  ( 5.000000000000000000, -4.685197434473812983, 6.938893903907228378E-15 ) ) ;
#219=EDGE_LOOP ( 'NONE', ( #7891, #2813, #3366 ) ) ;
#254=LINE ( 'NONE', #4112, #5840 ) ;
#284=ORIENTED_EDGE ( 'NONE', *, *, #6755, .T. ) ;
#285=CARTESIAN_POINT ( 'NONE',  ( 5.000000000000000000, 2.342598717236912265, 4.057499999999998330 ) ) ;
#298=CARTESIAN_POINT ( 'NONE',  ( 10.00000000000000000, 0.000000000000000000, -5.400000000000001243 ) ) ;
#299=ORIENTED_EDGE ( 'NONE', *, *, #10711, .T. ) ;
#329=FACE_OUTER_BOUND ( 'NONE', #219, .T. ) ;
#351=ORIENTED_EDGE ( 'NONE', *, *, #11716, .T. ) ;
#378=VERTEX_POINT ( 'NONE', #285 ) ;
#394=EDGE_LOOP ( 'NONE', ( #5603, #4976 ) ) ;
#407=ORIENTED_EDGE ( 'NONE', *, *, #9717, .F. ) ;
#430=VECTOR ( 'NONE', #1813, 999.9999999999998863 ) ;
#431=( LENGTH_UNIT ( ) NAMED_UNIT ( * ) SI_UNIT ( .MILLI., .METRE. ) );
#472=FACE_BOUND ( 'NONE', #10780, .T. ) ;
#506=VECTOR ( 'NONE', #2132, 1000.000000000000000 ) ;
#535=DIRECTION ( 'NONE',  ( 0.000000000000000000, 0.000000000000000000, 1.000000000000000000 ) ) ;
#539=CARTESIAN_POINT ( 'NONE',  ( 0.000000000000000000, 0.000000000000000000, 0.000000000000000000 ) ) ;
#541=ORIENTED_EDGE ( 'NONE', *, *, #3157, .F. ) ;
#570=ADVANCED_FACE ( 'NONE', ( #472, #5485 ), #8212, .T. ) ;
#594=DIRECTION ( 'NONE',  ( 0.000000000000000000, -0.5000000000000009992, -0.8660254037844380415 ) ) ;
#649=ORIENTED_EDGE ( 'NONE', *, *, #2660, .F. ) ;
#667=VERTEX_POINT ( 'NONE', #3941 ) ;
#672=CYLINDRICAL_SURFACE ( 'NONE', #85, 8.000000000000000000 ) ;
#673=AXIS2_PLACEMENT_3D ( 'NONE', #4631, #7426, #822 ) ;
#681=PLANE ( 'NONE',  #9133 ) ;
#685=LINE ( 'NONE', #8552, #3386 ) ;
#688=CONICAL_SURFACE ( 'NONE', #7982, 4.057500000000000107, 1.047197551196593857 ) ;
#709=AXIS2_PLACEMENT_3D ( 'NONE', #12100, #12221, #7145 ) ;
#718=DIRECTION ( 'NONE',  ( 0.000000000000000000, 0.000000000000000000, -1.000000000000000000 ) ) ;
#738=LINE ( 'NONE', #9227, #506 ) ;
#758=ORIENTED_EDGE ( 'NONE', *, *, #7126, .F. ) ;
#759=DIRECTION ( 'NONE',  ( 0.000000000000000000, 1.000000000000000000, -1.295896757998781374E-15 ) ) ;
#765=CARTESIAN_POINT ( 'NONE',  ( 5.000000000000000000, 4.685197434473814759, -5.637851296924623057E-15 ) ) ;
#767=ORIENTED_EDGE ( 'NONE', *, *, #1303, .T. ) ;
#771=PRODUCT_DEFINITION ( 'UNKNOWN', '', #6364, #5110 ) ;
#798=CLOSED_SHELL ( 'NONE', ( #7102, #11031, #3425, #12222, #9856, #7107, #9235, #2450, #570, #3722, #6454, #5883, #7818, #6592, #5655, #2029, #10833, #3408, #1229, #5066, #2806, #9157, #3585, #11147, #6385, #11013, #2555 ) ) ;
#822=DIRECTION ( 'NONE',  ( 0.000000000000000000, 0.000000000000000000, 1.000000000000000000 ) ) ;
#858=DIRECTION ( 'NONE',  ( 0.000000000000000000, 0.000000000000000000, 1.000000000000000000 ) ) ;
#868=EDGE_CURVE ( 'NONE', #10579, #6723, #10784, .T. ) ;
#869=EDGE_LOOP ( 'NONE', ( #5985, #11323, #8486, #2065, #3594 ) ) ;
#875=CARTESIAN_POINT ( 'NONE',  ( 10.00000000000000178, 0.000000000000000000, 0.000000000000000000 ) ) ;
#904=CARTESIAN_POINT ( 'NONE',  ( 5.000000000000000000, 0.000000000000000000, 0.000000000000000000 ) ) ;
#927=FACE_OUTER_BOUND ( 'NONE', #11549, .T. ) ;
#930=EDGE_CURVE ( 'NONE', #5431, #4145, #2846, .T. ) ;
#988=CARTESIAN_POINT ( 'NONE',  ( -31.74999999999995737, 9.797174393178825657E-16, -8.000000000000000000 ) ) ;
#996=ORIENTED_EDGE ( 'NONE', *, *, #8532, .T. ) ;
#1015=DIRECTION ( 'NONE',  ( 0.000000000000000000, -0.4999999999999990008, 0.8660254037844391517 ) ) ;
#1029=EDGE_CURVE ( 'NONE', #667, #12368, #11254, .T. ) ;
#1086=LINE ( 'NONE', #2158, #7277 ) ;
#1090=DIRECTION ( 'NONE',  ( -1.000000000000000000, -0.000000000000000000, -0.000000000000000000 ) ) ;
#1131=CARTESIAN_POINT ( 'NONE',  ( 0.000000000000000000, -2.342598717236902051, 4.057500000000004547 ) ) ;
#1188=ORIENTED_EDGE ( 'NONE', *, *, #5383, .T. ) ;
#1229=ADVANCED_FACE ( 'NONE', ( #2519 ), #10255, .F. ) ;
#1234=ORIENTED_EDGE ( 'NONE', *, *, #5145, .F. ) ;
#1235=LINE ( 'NONE', #3713, #430 ) ;
#1236=ORIENTED_EDGE ( 'NONE', *, *, #4278, .T. ) ;
#1245=ORIENTED_EDGE ( 'NONE', *, *, #6971, .T. ) ;
#1253=ORIENTED_EDGE ( 'NONE', *, *, #10753, .F. ) ;
#1293=CIRCLE ( 'NONE', #9192, 5.000000000000000888 ) ;
#1303=EDGE_CURVE ( 'NONE', #5355, #12320, #3557, .T. ) ;
#1361=DIRECTION ( 'NONE',  ( -1.000000000000000000, -0.000000000000000000, -0.000000000000000000 ) ) ;
#1379=CIRCLE ( 'NONE', #5423, 4.057500000000000107 ) ;
#1384=DIRECTION ( 'NONE',  ( 0.000000000000000000, 0.000000000000000000, 1.000000000000000000 ) ) ;
#1426=VERTEX_POINT ( 'NONE', #6191 ) ;
#1430=VECTOR ( 'NONE', #5911, 999.9999999999998863 ) ;
#1439=CARTESIAN_POINT ( 'NONE',  ( 5.000000000000000000, -2.342598717236902051, 4.057500000000004547 ) ) ;
#1447=( NAMED_UNIT ( * ) SI_UNIT ( $, .STERADIAN. ) SOLID_ANGLE_UNIT ( ) );
#1485=DIRECTION ( 'NONE',  ( -1.000000000000000000, -0.000000000000000000, -0.000000000000000000 ) ) ;
#1491=EDGE_LOOP ( 'NONE', ( #541, #9972, #12260, #5849, #3995 ) ) ;
#1497=ORIENTED_EDGE ( 'NONE', *, *, #1029, .F. ) ;
#1511=EDGE_LOOP ( 'NONE', ( #11700, #4285, #649, #5260, #9716 ) ) ;
#1520=FACE_OUTER_BOUND ( 'NONE', #5559, .T. ) ;
#1521=VERTEX_POINT ( 'NONE', #6886 ) ;
#1566=APPLICATION_CONTEXT ( 'automotive_design' ) ;
#1570=DIRECTION ( 'NONE',  ( 0.000000000000000000, -0.8660254037844392627, -0.4999999999999990008 ) ) ;
#1572=DIRECTION ( 'NONE',  ( 0.000000000000000000, 0.000000000000000000, 1.000000000000000000 ) ) ;
#1582=CARTESIAN_POINT ( 'NONE',  ( 5.000000000000000000, -2.342598717236902051, 4.057500000000004547 ) ) ;
#1587=ORIENTED_EDGE ( 'NONE', *, *, #2660, .T. ) ;
#1596=LINE ( 'NONE', #10278, #4640 ) ;
#1601=EDGE_LOOP ( 'NONE', ( #10052, #6468, #11504, #299, #2507, #758 ) ) ;
#1607=FACE_BOUND ( 'NONE', #1601, .T. ) ;
#1677=EDGE_CURVE ( 'NONE', #2800, #2324, #10246, .T. ) ;
#1723=VERTEX_POINT ( 'NONE', #11259 ) ;
#1756=DIRECTION ( 'NONE',  ( 0.000000000000000000, 0.000000000000000000, 1.000000000000000000 ) ) ;
#1763=AXIS2_PLACEMENT_3D ( 'NONE', #8719, #2949, #2051 ) ;
#1792=LINE ( 'NONE', #8464, #9290 ) ;
#1813=DIRECTION ( 'NONE',  ( 0.000000000000000000, -0.5000000000000014433, -0.8660254037844379305 ) ) ;
#1815=EDGE_LOOP ( 'NONE', ( #10593, #7293, #1188, #106 ) ) ;
#1847=CARTESIAN_POINT ( 'NONE',  ( 0.000000000000000000, 0.000000000000000000, 0.000000000000000000 ) ) ;
#1867=DIRECTION ( 'NONE',  ( -1.000000000000000000, -0.000000000000000000, -0.000000000000000000 ) ) ;
#1924=TOROIDAL_SURFACE ( 'NONE', #8612, 6.500000000000000888, 1.500000000000000000 ) ;
#1966=CARTESIAN_POINT ( 'NONE',  ( 1.500000000000001332, 9.797174393178825657E-16, -8.000000000000000000 ) ) ;
#2010=DIRECTION ( 'NONE',  ( -1.000000000000000000, -0.000000000000000000, -0.000000000000000000 ) ) ;
#2029=ADVANCED_FACE ( 'NONE', ( #11256 ), #3275, .F. ) ;
#2051=DIRECTION ( 'NONE',  ( 0.000000000000000000, 0.000000000000000000, 1.000000000000000000 ) ) ;
#2065=ORIENTED_EDGE ( 'NONE', *, *, #5531, .T. ) ;
#2092=DIRECTION ( 'NONE',  ( 0.000000000000000000, 0.000000000000000000, 1.000000000000000000 ) ) ;
#2095=CARTESIAN_POINT ( 'NONE',  ( 10.00000000000000178, 9.797174393178825657E-16, -8.000000000000000000 ) ) ;
#2108=VERTEX_POINT ( 'NONE', #8589 ) ;
#2130=AXIS2_PLACEMENT_3D ( 'NONE', #11454, #2761, #2825 ) ;
#2132=DIRECTION ( 'NONE',  ( 0.000000000000000000, -1.000000000000000000, 1.110768649713241713E-15 ) ) ;
#2137=AXIS2_PLACEMENT_3D ( 'NONE', #4802, #2768, #3905 ) ;
#2138=FACE_OUTER_BOUND ( 'NONE', #12282, .T. ) ;
#2158=CARTESIAN_POINT ( 'NONE',  ( 5.000000000000000000, 4.685197434473814759, -5.637851296924623057E-15 ) ) ;
#2165=CIRCLE ( 'NONE', #11477, 0.4000000000000001887 ) ;
#2192=CARTESIAN_POINT ( 'NONE',  ( 90.00000000000000000, 4.171999999999999709, 0.000000000000000000 ) ) ;
#2195=ORIENTED_EDGE ( 'NONE', *, *, #4213, .T. ) ;
#2206=CIRCLE ( 'NONE', #10910, 8.000000000000000000 ) ;
#2220=CONICAL_SURFACE ( 'NONE', #3510, 4.171999999999999709, 0.7853981633974609355 ) ;
#2276=DIRECTION ( 'NONE',  ( 1.000000000000000000, 0.000000000000000000, 0.000000000000000000 ) ) ;
#2293=ORIENTED_EDGE ( 'NONE', *, *, #6989, .F. ) ;
#2321=ORIENTED_EDGE ( 'NONE', *, *, #8532, .F. ) ;
#2324=VERTEX_POINT ( 'NONE', #4329 ) ;
#2336=CARTESIAN_POINT ( 'NONE',  ( 90.00000000000000000, 0.000000000000000000, 0.000000000000000000 ) ) ;
#2341=EDGE_CURVE ( 'NONE', #6176, #6723, #3452, .T. ) ;
#2349=AXIS2_PLACEMENT_3D ( 'NONE', #5446, #4485, #10688 ) ;
#2402=AXIS2_PLACEMENT_3D ( 'NONE', #6387, #1570, #10251 ) ;
#2407=ORIENTED_EDGE ( 'NONE', *, *, #930, .T. ) ;
#2412=ORIENTED_EDGE ( 'NONE', *, *, #4212, .T. ) ;
#2447=AXIS2_PLACEMENT_3D ( 'NONE', #10998, #3379, #9225 ) ;
#2450=ADVANCED_FACE ( 'NONE', ( #6480 ), #4701, .T. ) ;
#2470=ORIENTED_EDGE ( 'NONE', *, *, #5986, .T. ) ;
#2482=ORIENTED_EDGE ( 'NONE', *, *, #11027, .F. ) ;
#2501=DIRECTION ( 'NONE',  ( 0.000000000000000000, 1.000000000000000000, -1.295896757998781374E-15 ) ) ;
#2507=ORIENTED_EDGE ( 'NONE', *, *, #1677, .F. ) ;
#2510=VECTOR ( 'NONE', #11080, 999.9999999999998863 ) ;
#2516=FACE_OUTER_BOUND ( 'NONE', #2630, .T. ) ;
#2519=FACE_OUTER_BOUND ( 'NONE', #6320, .T. ) ;
#2521=FACE_OUTER_BOUND ( 'NONE', #869, .T. ) ;
#2522=ORIENTED_EDGE ( 'NONE', *, *, #10958, .T. ) ;
#2529=LINE ( 'NONE', #3421, #11092 ) ;
#2534=CARTESIAN_POINT ( 'NONE',  ( 89.17200000000001125, 0.000000000000000000, 5.000000000000001776 ) ) ;
#2550=VERTEX_POINT ( 'NONE', #1966 ) ;
#2555=ADVANCED_FACE ( 'NONE', ( #11615 ), #8717, .F. ) ;
#2560=DIRECTION ( 'NONE',  ( -1.000000000000000000, -0.000000000000000000, -0.000000000000000000 ) ) ;
#2568=VECTOR ( 'NONE', #12453, 1000.000000000000000 ) ;
#2591=DIRECTION ( 'NONE',  ( 0.000000000000000000, -0.5000000000000009992, -0.8660254037844380415 ) ) ;
#2593=AXIS2_PLACEMENT_3D ( 'NONE', #6469, #11292, #2664 ) ;
#2599=AXIS2_PLACEMENT_3D ( 'NONE', #875, #9572, #1756 ) ;
#2614=CARTESIAN_POINT ( 'NONE',  ( -31.74999999999995737, 0.000000000000000000, 0.000000000000000000 ) ) ;
#2630=EDGE_LOOP ( 'NONE', ( #8653, #6116, #9080, #4636, #11908 ) ) ;
#2646=CARTESIAN_POINT ( 'NONE',  ( 5.000000000000000000, -4.685197434473812983, 6.938893903907228378E-15 ) ) ;
#2652=DIRECTION ( 'NONE',  ( -0.5000000000000034417, 1.060575238724904696E-16, -0.8660254037844367092 ) ) ;
#2660=EDGE_CURVE ( 'NONE', #1521, #8006, #6722, .T. ) ;
#2664=DIRECTION ( 'NONE',  ( 0.000000000000000000, 0.000000000000000000, -1.000000000000000000 ) ) ;
#2703=CARTESIAN_POINT ( 'NONE',  ( 90.00000000000000000, 0.000000000000000000, 0.000000000000000000 ) ) ;
#2721=DIRECTION ( 'NONE',  ( 0.000000000000000000, 0.000000000000000000, 1.000000000000000000 ) ) ;
#2737=AXIS2_PLACEMENT_3D ( 'NONE', #3284, #10074, #1384 ) ;
#2744=DIRECTION ( 'NONE',  ( 0.000000000000000000, 0.000000000000000000, 1.000000000000000000 ) ) ;
#2761=DIRECTION ( 'NONE',  ( -1.000000000000000000, -0.000000000000000000, -0.000000000000000000 ) ) ;
#2768=DIRECTION ( 'NONE',  ( 0.000000000000000000, -1.000000000000000000, 0.000000000000000000 ) ) ;
#2783=CARTESIAN_POINT ( 'NONE',  ( 5.000000000000000000, -2.342598717236902051, 4.057500000000004547 ) ) ;
#2800=VERTEX_POINT ( 'NONE', #7041 ) ;
#2806=ADVANCED_FACE ( 'NONE', ( #329 ), #4313, .F. ) ;
#2813=ORIENTED_EDGE ( 'NONE', *, *, #5531, .F. ) ;
#2825=DIRECTION ( 'NONE',  ( 0.000000000000000000, 0.000000000000000000, 1.000000000000000000 ) ) ;
#2833=FACE_OUTER_BOUND ( 'NONE', #9349, .T. ) ;
#2846=LINE ( 'NONE', #56, #11453 ) ;
#2889=DIRECTION ( 'NONE',  ( 0.000000000000000000, 0.000000000000000000, -1.000000000000000000 ) ) ;
#2892=DIRECTION ( 'NONE',  ( -1.000000000000000000, -0.000000000000000000, -0.000000000000000000 ) ) ;
#2897=UNCERTAINTY_MEASURE_WITH_UNIT (LENGTH_MEASURE( 1.000000000000000082E-05 ), #431, 'distance_accuracy_value', 'NONE');
#2924=ORIENTED_EDGE ( 'NONE', *, *, #8828, .T. ) ;
#2949=DIRECTION ( 'NONE',  ( -1.000000000000000000, -0.000000000000000000, -0.000000000000000000 ) ) ;
#3020=ORIENTED_EDGE ( 'NONE', *, *, #11242, .F. ) ;
#3038=PRODUCT_CONTEXT ( 'NONE', #1566, 'mechanical' ) ;
#3069=ORIENTED_EDGE ( 'NONE', *, *, #10523, .T. ) ;
#3086=CYLINDRICAL_SURFACE ( 'NONE', #11276, 5.000000000000000888 ) ;
#3125=CARTESIAN_POINT ( 'NONE',  ( 5.000000000000000000, 4.685197434473814759, -5.637851296924623057E-15 ) ) ;
#3149=LINE ( 'NONE', #1131, #3937 ) ;
#3157=EDGE_CURVE ( 'NONE', #7779, #6828, #5956, .T. ) ;
#3210=VECTOR ( 'NONE', #2501, 1000.000000000000000 ) ;
#3214=ORIENTED_EDGE ( 'NONE', *, *, #5340, .F. ) ;
#3259=ORIENTED_EDGE ( 'NONE', *, *, #12481, .F. ) ;
#3275=PLANE ( 'NONE',  #8884 ) ;
#3284=CARTESIAN_POINT ( 'NONE',  ( 1.500000000000001332, 0.000000000000000000, 0.000000000000000000 ) ) ;
#3339=CARTESIAN_POINT ( 'NONE',  ( 0.000000000000000000, 4.685197434473814759, -5.637851296924623057E-15 ) ) ;
#3341=CARTESIAN_POINT ( 'NONE',  ( 5.000000000000000000, -4.685197434473812983, 6.938893903907228378E-15 ) ) ;
#3365=DIRECTION ( 'NONE',  ( -1.000000000000000000, -0.000000000000000000, -0.000000000000000000 ) ) ;
#3366=ORIENTED_EDGE ( 'NONE', *, *, #2341, .F. ) ;
#3379=DIRECTION ( 'NONE',  ( 1.000000000000000000, 0.000000000000000000, 0.000000000000000000 ) ) ;
#3386=VECTOR ( 'NONE', #2652, 999.9999999999998863 ) ;
#3405=CARTESIAN_POINT ( 'NONE',  ( 5.000000000000000000, -2.342598717236911821, -4.057499999999996554 ) ) ;
#3408=ADVANCED_FACE ( 'NONE', ( #2521 ), #681, .T. ) ;
#3421=CARTESIAN_POINT ( 'NONE',  ( -31.74999999999995737, 6.123233995736767268E-16, -5.000000000000000888 ) ) ;
#3425=ADVANCED_FACE ( 'NONE', ( #2833 ), #3648, .F. ) ;
#3452=CIRCLE ( 'NONE', #5685, 4.057500000000000107 ) ;
#3467=( NAMED_UNIT ( * ) PLANE_ANGLE_UNIT ( ) SI_UNIT ( $, .RADIAN. ) );
#3507=EDGE_CURVE ( 'NONE', #6002, #1521, #1235, .T. ) ;
#3510=AXIS2_PLACEMENT_3D ( 'NONE', #7667, #5583, #2721 ) ;
#3523=FACE_OUTER_BOUND ( 'NONE', #1815, .T. ) ;
#3530=DIRECTION ( 'NONE',  ( -0.000000000000000000, 0.8660254037844393737, 0.4999999999999987788 ) ) ;
#3557=CIRCLE ( 'NONE', #2137, 1.499999999999999556 ) ;
#3585=ADVANCED_FACE ( 'NONE', ( #9287 ), #7124, .F. ) ;
#3594=ORIENTED_EDGE ( 'NONE', *, *, #9449, .T. ) ;
#3646=DIRECTION ( 'NONE',  ( 0.000000000000000000, 0.000000000000000000, 1.000000000000000000 ) ) ;
#3648=TOROIDAL_SURFACE ( 'NONE', #8135, 5.400000000000001243, 0.4000000000000000222 ) ;
#3650=DIRECTION ( 'NONE',  ( 0.000000000000000000, 0.000000000000000000, -1.000000000000000000 ) ) ;
#3670=ORIENTED_EDGE ( 'NONE', *, *, #10391, .F. ) ;
#3695=ORIENTED_EDGE ( 'NONE', *, *, #6971, .F. ) ;
#3713=CARTESIAN_POINT ( 'NONE',  ( 5.000000000000000000, 4.685197434473814759, -5.637851296924623057E-15 ) ) ;
#3719=DIRECTION ( 'NONE',  ( 0.000000000000000000, 0.000000000000000000, 1.000000000000000000 ) ) ;
#3722=ADVANCED_FACE ( 'NONE', ( #10469 ), #6482, .T. ) ;
#3728=ORIENTED_EDGE ( 'NONE', *, *, #9717, .T. ) ;
#3743=CARTESIAN_POINT ( 'NONE',  ( -31.74999999999995737, 0.000000000000000000, 0.000000000000000000 ) ) ;
#3744=ORIENTED_EDGE ( 'NONE', *, *, #1029, .T. ) ;
#3746=ORIENTED_EDGE ( 'NONE', *, *, #4038, .T. ) ;
#3770=FACE_OUTER_BOUND ( 'NONE', #6842, .T. ) ;
#3838=DIRECTION ( 'NONE',  ( 1.000000000000000000, 0.000000000000000000, 0.000000000000000000 ) ) ;
#3844=VERTEX_POINT ( 'NONE', #2095 ) ;
#3905=DIRECTION ( 'NONE',  ( 0.000000000000000000, 0.000000000000000000, -1.000000000000000000 ) ) ;
#3916=AXIS2_PLACEMENT_3D ( 'NONE', #2336, #12225, #4363 ) ;
#3937=VECTOR ( 'NONE', #594, 1000.000000000000114 ) ;
#3941=CARTESIAN_POINT ( 'NONE',  ( 10.40000000000000036, 0.000000000000000000, 5.000000000000000888 ) ) ;
#3948=AXIS2_PLACEMENT_3D ( 'NONE', #5691, #1867, #858 ) ;
#3977=DIRECTION ( 'NONE',  ( 0.000000000000000000, 0.000000000000000000, 1.000000000000000000 ) ) ;
#3995=ORIENTED_EDGE ( 'NONE', *, *, #10753, .T. ) ;
#4015=VECTOR ( 'NONE', #7321, 1000.000000000000114 ) ;
#4024=UNCERTAINTY_MEASURE_WITH_UNIT (LENGTH_MEASURE( 1.000000000000000082E-05 ), #12066, 'distance_accuracy_value', 'NONE');
#4038=EDGE_CURVE ( 'NONE', #1723, #1521, #12184, .T. ) ;
#4062=EDGE_LOOP ( 'NONE', ( #11400, #5448 ) ) ;
#4065=DIRECTION ( 'NONE',  ( 0.000000000000000000, 0.4999999999999987232, -0.8660254037844392627 ) ) ;
#4099=DIRECTION ( 'NONE',  ( 0.000000000000000000, 1.000000000000000000, -1.224646799147353207E-16 ) ) ;
#4103=DIRECTION ( 'NONE',  ( 0.000000000000000000, 0.000000000000000000, -1.000000000000000000 ) ) ;
#4112=CARTESIAN_POINT ( 'NONE',  ( 0.000000000000000000, 4.685197434473814759, -5.637851296924623057E-15 ) ) ;
#4120=DIRECTION ( 'NONE',  ( 0.000000000000000000, -0.4999999999999990008, 0.8660254037844391517 ) ) ;
#4125=ORIENTED_EDGE ( 'NONE', *, *, #1303, .F. ) ;
#4145=VERTEX_POINT ( 'NONE', #2534 ) ;
#4158=EDGE_LOOP ( 'NONE', ( #11462, #1236, #8774, #9016 ) ) ;
#4168=VECTOR ( 'NONE', #4065, 1000.000000000000227 ) ;
#4210=CARTESIAN_POINT ( 'NONE',  ( 5.000000000000000000, 0.000000000000000000, 0.000000000000000000 ) ) ;
#4212=EDGE_CURVE ( 'NONE', #12368, #6993, #8674, .T. ) ;
#4213=EDGE_CURVE ( 'NONE', #10247, #6828, #12371, .T. ) ;
#4233=VECTOR ( 'NONE', #12056, 1000.000000000000000 ) ;
#4234=DIRECTION ( 'NONE',  ( 0.000000000000000000, 1.224646799147353207E-16, 1.000000000000000000 ) ) ;
#4278=EDGE_CURVE ( 'NONE', #169, #9642, #5833, .T. ) ;
#4285=ORIENTED_EDGE ( 'NONE', *, *, #10468, .F. ) ;
#4313=PLANE ( 'NONE',  #11975 ) ;
#4329=CARTESIAN_POINT ( 'NONE',  ( 0.000000000000000000, -2.342598717236911821, -4.057499999999996554 ) ) ;
#4350=DIRECTION ( 'NONE',  ( 0.000000000000000000, -1.000000000000000000, 1.295896757998781572E-15 ) ) ;
#4363=DIRECTION ( 'NONE',  ( 0.000000000000000000, 0.000000000000000000, 1.000000000000000000 ) ) ;
#4366=ORIENTED_EDGE ( 'NONE', *, *, #6755, .F. ) ;
#4379=ORIENTED_EDGE ( 'NONE', *, *, #6506, .F. ) ;
#4394=CARTESIAN_POINT ( 'NONE',  ( 10.40000000000000036, 6.123233995736767268E-16, -5.000000000000000888 ) ) ;
#4403=CARTESIAN_POINT ( 'NONE',  ( 5.000000000000000000, -2.342598717236902051, 4.057500000000004547 ) ) ;
#4407=EDGE_LOOP ( 'NONE', ( #12, #12317, #4769, #3746, #284 ) ) ;
#4424=EDGE_CURVE ( 'NONE', #9969, #11906, #254, .T. ) ;
#4442=( NAMED_UNIT ( * ) SI_UNIT ( $, .STERADIAN. ) SOLID_ANGLE_UNIT ( ) );
#4469=ORIENTED_EDGE ( 'NONE', *, *, #4882, .F. ) ;
#4475=CARTESIAN_POINT ( 'NONE',  ( 90.00000000000000000, 5.616230220889762438E-16, -4.171999999999999709 ) ) ;
#4485=DIRECTION ( 'NONE',  ( 0.000000000000000000, -1.110768649713241713E-15, -1.000000000000000000 ) ) ;
#4499=ORIENTED_EDGE ( 'NONE', *, *, #1677, .T. ) ;
#4526=AXIS2_PLACEMENT_3D ( 'NONE', #8998, #5132, #8804 ) ;
#4534=DIRECTION ( 'NONE',  ( 0.000000000000000000, -1.000000000000000000, 1.110768649713241713E-15 ) ) ;
#4620=LINE ( 'NONE', #6641, #10796 ) ;
#4631=CARTESIAN_POINT ( 'NONE',  ( 89.17200000000001125, 0.000000000000000000, 0.000000000000000000 ) ) ;
#4636=ORIENTED_EDGE ( 'NONE', *, *, #6111, .T. ) ;
#4640=VECTOR ( 'NONE', #10947, 1000.000000000000000 ) ;
#4642=ORIENTED_EDGE ( 'NONE', *, *, #8971, .F. ) ;
#4643=VECTOR ( 'NONE', #7266, 1000.000000000000000 ) ;
#4658=EDGE_LOOP ( 'NONE', ( #12076, #996, #1245, #12536 ) ) ;
#4679=EDGE_CURVE ( 'NONE', #1426, #11906, #11193, .T. ) ;
#4701=CYLINDRICAL_SURFACE ( 'NONE', #12165, 8.000000000000000000 ) ;
#4728=LINE ( 'NONE', #8477, #10427 ) ;
#4750=EDGE_CURVE ( 'NONE', #10247, #12336, #11903, .T. ) ;
#4769=ORIENTED_EDGE ( 'NONE', *, *, #9171, .T. ) ;
#4775=DIRECTION ( 'NONE',  ( -0.000000000000000000, 0.000000000000000000, 1.000000000000000000 ) ) ;
#4795=CARTESIAN_POINT ( 'NONE',  ( 5.000000000000000000, 4.685197434473814759, -5.637851296924623057E-15 ) ) ;
#4802=CARTESIAN_POINT ( 'NONE',  ( 1.500000000000001332, 0.000000000000000000, 6.500000000000000888 ) ) ;
#4807=VERTEX_POINT ( 'NONE', #8280 ) ;
#4869=ORIENTED_EDGE ( 'NONE', *, *, #11716, .F. ) ;
#4882=EDGE_CURVE ( 'NONE', #378, #11906, #1792, .T. ) ;
#4905=CARTESIAN_POINT ( 'NONE',  ( 5.000000000000000000, 2.342598717236900718, -4.057500000000001883 ) ) ;
#4934=AXIS2_PLACEMENT_3D ( 'NONE', #10685, #10886, #4990 ) ;
#4936=FACE_OUTER_BOUND ( 'NONE', #8651, .T. ) ;
#4954=EDGE_LOOP ( 'NONE', ( #3214, #2482 ) ) ;
#4976=ORIENTED_EDGE ( 'NONE', *, *, #6815, .F. ) ;
#4986=DIRECTION ( 'NONE',  ( 1.000000000000000000, 0.000000000000000000, 0.000000000000000000 ) ) ;
#4990=DIRECTION ( 'NONE',  ( 0.000000000000000000, -1.224646799147353454E-16, 1.000000000000000000 ) ) ;
#4998=DIRECTION ( 'NONE',  ( 0.000000000000000000, 0.000000000000000000, 1.000000000000000000 ) ) ;
#5001=DIRECTION ( 'NONE',  ( 1.000000000000000000, 0.000000000000000000, 0.000000000000000000 ) ) ;
#5010=CIRCLE ( 'NONE', #8856, 5.400000000000001243 ) ;
#5066=ADVANCED_FACE ( 'NONE', ( #11694 ), #7952, .F. ) ;
#5088=EDGE_LOOP ( 'NONE', ( #5679, #4469, #1234, #7909, #2924 ) ) ;
#5110=PRODUCT_DEFINITION_CONTEXT ( 'detailed design', #11049, 'design' ) ;
#5132=DIRECTION ( 'NONE',  ( -1.000000000000000000, -0.000000000000000000, -0.000000000000000000 ) ) ;
#5145=EDGE_CURVE ( 'NONE', #6828, #378, #7287, .T. ) ;
#5213=ORIENTED_EDGE ( 'NONE', *, *, #4750, .T. ) ;
#5238=DIRECTION ( 'NONE',  ( 0.000000000000000000, 0.000000000000000000, 1.000000000000000000 ) ) ;
#5260=ORIENTED_EDGE ( 'NONE', *, *, #3507, .F. ) ;
#5264=CARTESIAN_POINT ( 'NONE',  ( 0.000000000000000000, 4.685197434473814759, -5.637851296924623057E-15 ) ) ;
#5310=CARTESIAN_POINT ( 'NONE',  ( 0.000000000000000000, 2.342598717236900718, -4.057500000000001883 ) ) ;
#5340=EDGE_CURVE ( 'NONE', #12462, #3844, #7669, .T. ) ;
#5352=ORIENTED_EDGE ( 'NONE', *, *, #6989, .T. ) ;
#5355=VERTEX_POINT ( 'NONE', #12363 ) ;
#5377=DIRECTION ( 'NONE',  ( 0.000000000000000000, 0.000000000000000000, 1.000000000000000000 ) ) ;
#5383=EDGE_CURVE ( 'NONE', #2550, #5355, #2206, .T. ) ;
#5384=CARTESIAN_POINT ( 'NONE',  ( 5.000000000000000000, 0.000000000000000000, 0.000000000000000000 ) ) ;
#5423=AXIS2_PLACEMENT_3D ( 'NONE', #11764, #10875, #6056 ) ;
#5431=VERTEX_POINT ( 'NONE', #11850 ) ;
#5446=CARTESIAN_POINT ( 'NONE',  ( 5.000000000000000000, 2.342598717236900718, -4.057500000000001883 ) ) ;
#5448=ORIENTED_EDGE ( 'NONE', *, *, #8971, .T. ) ;
#5450=AXIS2_PLACEMENT_3D ( 'NONE', #3125, #9670, #6803 ) ;
#5454=EDGE_CURVE ( 'NONE', #6993, #4807, #6858, .T. ) ;
#5485=FACE_OUTER_BOUND ( 'NONE', #4954, .T. ) ;
#5486=DIRECTION ( 'NONE',  ( -1.000000000000000000, 0.000000000000000000, -0.000000000000000000 ) ) ;
#5497=ORIENTED_EDGE ( 'NONE', *, *, #9171, .F. ) ;
#5509=DIRECTION ( 'NONE',  ( -1.000000000000000000, -0.000000000000000000, -0.000000000000000000 ) ) ;
#5531=EDGE_CURVE ( 'NONE', #6723, #6737, #6140, .T. ) ;
#5548=DIRECTION ( 'NONE',  ( 1.000000000000000000, 0.000000000000000000, 0.000000000000000000 ) ) ;
#5559=EDGE_LOOP ( 'NONE', ( #4379, #9456, #10810 ) ) ;
#5561=VECTOR ( 'NONE', #9433, 1000.000000000000000 ) ;
#5566=FACE_OUTER_BOUND ( 'NONE', #4158, .T. ) ;
#5583=DIRECTION ( 'NONE',  ( -1.000000000000000000, -0.000000000000000000, -0.000000000000000000 ) ) ;
#5600=ORIENTED_EDGE ( 'NONE', *, *, #7210, .F. ) ;
#5603=ORIENTED_EDGE ( 'NONE', *, *, #11101, .F. ) ;
#5611=CARTESIAN_POINT ( 'NONE',  ( 0.000000000000000000, -4.685197434473812983, 6.938893903907228378E-15 ) ) ;
#5626=CARTESIAN_POINT ( 'NONE',  ( 5.000000000000000000, 5.258101095580057891E-15, 4.057500000000001883 ) ) ;
#5655=ADVANCED_FACE ( 'NONE', ( #2516 ), #10012, .T. ) ;
#5679=ORIENTED_EDGE ( 'NONE', *, *, #4679, .T. ) ;
#5685=AXIS2_PLACEMENT_3D ( 'NONE', #4210, #1361, #8083 ) ;
#5691=CARTESIAN_POINT ( 'NONE',  ( 90.00000000000000000, 0.000000000000000000, 0.000000000000000000 ) ) ;
#5721=EDGE_LOOP ( 'NONE', ( #407, #3695, #2412, #3670 ) ) ;
#5739=CIRCLE ( 'NONE', #673, 5.000000000000001776 ) ;
#5783=PRODUCT ( 'socket head cap screw_iso_ISO 4762 M10 x 80 - 32N', 'socket head cap screw_iso_ISO 4762 M10 x 80 - 32N', '', ( #3038 ) ) ;
#5825=CIRCLE ( 'NONE', #7654, 4.057500000000000107 ) ;
#5832=EDGE_LOOP ( 'NONE', ( #12243, #2195, #1253 ) ) ;
#5833=LINE ( 'NONE', #6711, #10693 ) ;
#5840=VECTOR ( 'NONE', #7030, 1000.000000000000114 ) ;
#5845=ORIENTED_EDGE ( 'NONE', *, *, #11027, .T. ) ;
#5849=ORIENTED_EDGE ( 'NONE', *, *, #8928, .T. ) ;
#5883=ADVANCED_FACE ( 'NONE', ( #7900 ), #5936, .T. ) ;
#5884=EDGE_LOOP ( 'NONE', ( #5600, #5845, #12186, #2522 ) ) ;
#5900=EDGE_CURVE ( 'NONE', #12462, #5355, #8786, .T. ) ;
#5911=DIRECTION ( 'NONE',  ( 0.000000000000000000, -0.5000000000000014433, -0.8660254037844379305 ) ) ;
#5936=PLANE ( 'NONE',  #8491 ) ;
#5949=CARTESIAN_POINT ( 'NONE',  ( 10.00000000000000000, 0.000000000000000000, 0.000000000000000000 ) ) ;
#5956=LINE ( 'NONE', #6841, #12171 ) ;
#5977=CARTESIAN_POINT ( 'NONE',  ( 7.342598717236928252, 0.000000000000000000, 0.000000000000000000 ) ) ;
#5985=ORIENTED_EDGE ( 'NONE', *, *, #10711, .F. ) ;
#5986=EDGE_CURVE ( 'NONE', #8006, #6176, #1596, .T. ) ;
#5990=AXIS2_PLACEMENT_3D ( 'NONE', #11787, #2276, #9891 ) ;
#6002=VERTEX_POINT ( 'NONE', #765 ) ;
#6041=CARTESIAN_POINT ( 'NONE',  ( 10.40000000000000036, 0.000000000000000000, 0.000000000000000000 ) ) ;
#6056=DIRECTION ( 'NONE',  ( 0.000000000000000000, 0.000000000000000000, 1.000000000000000000 ) ) ;
#6073=AXIS2_PLACEMENT_3D ( 'NONE', #8312, #8681, #8557 ) ;
#6074=CARTESIAN_POINT ( 'NONE',  ( 10.00000000000000178, 0.000000000000000000, 8.000000000000000000 ) ) ;
#6111=EDGE_CURVE ( 'NONE', #1723, #378, #1086, .T. ) ;
#6116=ORIENTED_EDGE ( 'NONE', *, *, #145, .F. ) ;
#6122=SHAPE_REPRESENTATION ( 'socket head cap screw_iso_ISO 4762 M10 x 80 - 32N', ( #9021 ), #6962 ) ;
#6140=LINE ( 'NONE', #3341, #11120 ) ;
#6164=ORIENTED_EDGE ( 'NONE', *, *, #8928, .F. ) ;
#6176=VERTEX_POINT ( 'NONE', #8815 ) ;
#6182=AXIS2_PLACEMENT_3D ( 'NONE', #12530, #3838, #11580 ) ;
#6191=CARTESIAN_POINT ( 'NONE',  ( 0.000000000000000000, -2.342598717236902051, 4.057500000000004547 ) ) ;
#6193=ORIENTED_EDGE ( 'NONE', *, *, #10958, .F. ) ;
#6219=ORIENTED_EDGE ( 'NONE', *, *, #10468, .T. ) ;
#6226=SHAPE_REPRESENTATION_RELATIONSHIP ( 'NONE' , 'NONE' ,  #6122, #11414 ) ;
#6242=CARTESIAN_POINT ( 'NONE',  ( 0.000000000000000000, 0.000000000000000000, 0.000000000000000000 ) ) ;
#6320=EDGE_LOOP ( 'NONE', ( #4499, #8887, #10619, #89, #6219 ) ) ;
#6344=DIRECTION ( 'NONE',  ( 0.000000000000000000, 0.000000000000000000, -1.000000000000000000 ) ) ;
#6364=PRODUCT_DEFINITION_FORMATION_WITH_SPECIFIED_SOURCE ( 'ANY', '', #5783, .NOT_KNOWN. ) ;
#6376=EDGE_LOOP ( 'NONE', ( #11074, #4869, #6164 ) ) ;
#6385=ADVANCED_FACE ( 'NONE', ( #1520 ), #9269, .F. ) ;
#6387=CARTESIAN_POINT ( 'NONE',  ( 5.000000000000000000, 4.685197434473814759, -5.637851296924623057E-15 ) ) ;
#6440=CARTESIAN_POINT ( 'NONE',  ( 5.000000000000000000, 4.685197434473814759, -5.637851296924623057E-15 ) ) ;
#6454=ADVANCED_FACE ( 'NONE', ( #10390 ), #2220, .T. ) ;
#6468=ORIENTED_EDGE ( 'NONE', *, *, #4679, .F. ) ;
#6469=CARTESIAN_POINT ( 'NONE',  ( 10.40000000000000036, 0.000000000000000000, -5.400000000000001243 ) ) ;
#6480=FACE_OUTER_BOUND ( 'NONE', #5884, .T. ) ;
#6482=CYLINDRICAL_SURFACE ( 'NONE', #11772, 5.000000000000000888 ) ;
#6504=DIRECTION ( 'NONE',  ( 1.000000000000000000, 0.000000000000000000, 0.000000000000000000 ) ) ;
#6506=EDGE_CURVE ( 'NONE', #6002, #1723, #4620, .T. ) ;
#6513=LINE ( 'NONE', #12051, #7020 ) ;
#6538=DIRECTION ( 'NONE',  ( 0.000000000000000000, 0.000000000000000000, 1.000000000000000000 ) ) ;
#6542=CIRCLE ( 'NONE', #9594, 4.057500000000000107 ) ;
#6564=CIRCLE ( 'NONE', #12045, 6.500000000000000888 ) ;
#6592=ADVANCED_FACE ( 'NONE', ( #4936 ), #8176, .T. ) ;
#6620=VECTOR ( 'NONE', #11562, 1000.000000000000000 ) ;
#6637=CARTESIAN_POINT ( 'NONE',  ( 5.000000000000000000, 0.000000000000000000, 0.000000000000000000 ) ) ;
#6641=CARTESIAN_POINT ( 'NONE',  ( 5.000000000000000000, 4.685197434473814759, -5.637851296924623057E-15 ) ) ;
#6701=AXIS2_PLACEMENT_3D ( 'NONE', #12063, #3365, #7232 ) ;
#6711=CARTESIAN_POINT ( 'NONE',  ( 90.00000000000000000, 5.109226446042757607E-16, -4.171999999999999709 ) ) ;
#6722=LINE ( 'NONE', #7874, #1430 ) ;
#6723=VERTEX_POINT ( 'NONE', #11981 ) ;
#6737=VERTEX_POINT ( 'NONE', #3405 ) ;
#6755=EDGE_CURVE ( 'NONE', #1521, #6176, #6542, .T. ) ;
#6768=DIRECTION ( 'NONE',  ( -1.000000000000000000, -0.000000000000000000, -0.000000000000000000 ) ) ;
#6787=CIRCLE ( 'NONE', #2737, 8.000000000000000000 ) ;
#6788=CARTESIAN_POINT ( 'NONE',  ( 5.000000000000000000, 0.000000000000000000, 0.000000000000000000 ) ) ;
#6798=LINE ( 'NONE', #4905, #6620 ) ;
#6803=DIRECTION ( 'NONE',  ( 0.000000000000000000, 0.5000000000000014433, 0.8660254037844379305 ) ) ;
#6815=EDGE_CURVE ( 'NONE', #169, #5431, #12023, .T. ) ;
#6828=VERTEX_POINT ( 'NONE', #5626 ) ;
#6841=CARTESIAN_POINT ( 'NONE',  ( 5.000000000000000000, 0.000000000000000000, 4.057500000000000107 ) ) ;
#6842=EDGE_LOOP ( 'NONE', ( #1587, #2470, #4366 ) ) ;
#6858=CIRCLE ( 'NONE', #10113, 5.400000000000001243 ) ;
#6886=CARTESIAN_POINT ( 'NONE',  ( 5.000000000000000000, 3.513898075855356851, -2.028750000000006271 ) ) ;
#6942=ORIENTED_EDGE ( 'NONE', *, *, #6111, .F. ) ;
#6962=( GEOMETRIC_REPRESENTATION_CONTEXT ( 3 ) GLOBAL_UNCERTAINTY_ASSIGNED_CONTEXT ( ( #4024 ) ) GLOBAL_UNIT_ASSIGNED_CONTEXT ( ( #12066, #7236, #4442 ) ) REPRESENTATION_CONTEXT ( 'NONE', 'WORKASPACE' ) );
#6967=SHAPE_DEFINITION_REPRESENTATION ( #9146, #6122 ) ;
#6971=EDGE_CURVE ( 'NONE', #12368, #667, #1293, .T. ) ;
#6989=EDGE_CURVE ( 'NONE', #2550, #2108, #74, .T. ) ;
#6993=VERTEX_POINT ( 'NONE', #298 ) ;
#7020=VECTOR ( 'NONE', #9381, 1000.000000000000000 ) ;
#7030=DIRECTION ( 'NONE',  ( 0.000000000000000000, -0.4999999999999990008, 0.8660254037844391517 ) ) ;
#7031=AXIS2_PLACEMENT_3D ( 'NONE', #1847, #5486, #4775 ) ;
#7041=CARTESIAN_POINT ( 'NONE',  ( 0.000000000000000000, 2.342598717236900718, -4.057500000000001883 ) ) ;
#7102=ADVANCED_FACE ( 'NONE', ( #8353 ), #688, .F. ) ;
#7107=ADVANCED_FACE ( 'NONE', ( #3523 ), #672, .T. ) ;
#7124=PLANE ( 'NONE',  #2447 ) ;
#7126=EDGE_CURVE ( 'NONE', #9969, #2800, #12037, .T. ) ;
#7145=DIRECTION ( 'NONE',  ( 0.000000000000000000, 0.5000000000000009992, 0.8660254037844380415 ) ) ;
#7203=CARTESIAN_POINT ( 'NONE',  ( 5.000000000000000000, 0.000000000000000000, 0.000000000000000000 ) ) ;
#7210=EDGE_CURVE ( 'NONE', #3844, #2550, #9680, .T. ) ;
#7232=DIRECTION ( 'NONE',  ( 0.000000000000000000, 0.000000000000000000, 1.000000000000000000 ) ) ;
#7236=( NAMED_UNIT ( * ) PLANE_ANGLE_UNIT ( ) SI_UNIT ( $, .RADIAN. ) );
#7242=CIRCLE ( 'NONE', #1763, 5.000000000000001776 ) ;
#7258=VECTOR ( 'NONE', #759, 1000.000000000000000 ) ;
#7266=DIRECTION ( 'NONE',  ( -1.000000000000000000, -0.000000000000000000, -0.000000000000000000 ) ) ;
#7277=VECTOR ( 'NONE', #4120, 1000.000000000000114 ) ;
#7287=LINE ( 'NONE', #11283, #4233 ) ;
#7293=ORIENTED_EDGE ( 'NONE', *, *, #7210, .T. ) ;
#7321=DIRECTION ( 'NONE',  ( 0.000000000000000000, -0.5000000000000009992, -0.8660254037844380415 ) ) ;
#7348=DIRECTION ( 'NONE',  ( -1.000000000000000000, -0.000000000000000000, -0.000000000000000000 ) ) ;
#7375=CARTESIAN_POINT ( 'NONE',  ( 0.000000000000000000, 0.000000000000000000, 6.500000000000000888 ) ) ;
#7426=DIRECTION ( 'NONE',  ( -1.000000000000000000, -0.000000000000000000, -0.000000000000000000 ) ) ;
#7467=DIRECTION ( 'NONE',  ( 0.000000000000000000, -0.4999999999999987232, 0.8660254037844392627 ) ) ;
#7504=FACE_OUTER_BOUND ( 'NONE', #6376, .T. ) ;
#7532=EDGE_LOOP ( 'NONE', ( #9427, #11342, #2407, #10425 ) ) ;
#7588=FACE_OUTER_BOUND ( 'NONE', #8796, .T. ) ;
#7648=DIRECTION ( 'NONE',  ( -1.000000000000000000, -0.000000000000000000, -0.000000000000000000 ) ) ;
#7654=AXIS2_PLACEMENT_3D ( 'NONE', #904, #8516, #10350 ) ;
#7667=CARTESIAN_POINT ( 'NONE',  ( 90.00000000000000000, 0.000000000000000000, 0.000000000000000000 ) ) ;
#7669=CIRCLE ( 'NONE', #2599, 8.000000000000000000 ) ;
#7700=ORIENTED_EDGE ( 'NONE', *, *, #10391, .T. ) ;
#7755=LINE ( 'NONE', #8354, #2568 ) ;
#7779=VERTEX_POINT ( 'NONE', #5977 ) ;
#7818=ADVANCED_FACE ( 'NONE', ( #17 ), #9582, .F. ) ;
#7874=CARTESIAN_POINT ( 'NONE',  ( 5.000000000000000000, 4.685197434473814759, -5.637851296924623057E-15 ) ) ;
#7881=DIRECTION ( 'NONE',  ( 1.000000000000000000, 0.000000000000000000, 0.000000000000000000 ) ) ;
#7891=ORIENTED_EDGE ( 'NONE', *, *, #12308, .T. ) ;
#7900=FACE_OUTER_BOUND ( 'NONE', #394, .T. ) ;
#7909=ORIENTED_EDGE ( 'NONE', *, *, #4213, .F. ) ;
#7911=CARTESIAN_POINT ( 'NONE',  ( 5.000000000000000000, -3.513898075855359071, 2.028750000000004494 ) ) ;
#7952=PLANE ( 'NONE',  #5450 ) ;
#7956=ORIENTED_EDGE ( 'NONE', *, *, #5145, .T. ) ;
#7959=DIRECTION ( 'NONE',  ( -1.000000000000000000, -0.000000000000000000, -0.000000000000000000 ) ) ;
#7982=AXIS2_PLACEMENT_3D ( 'NONE', #7203, #9372, #5377 ) ;
#8004=CONICAL_SURFACE ( 'NONE', #8402, 4.171999999999999709, 0.7853981633974609355 ) ;
#8006=VERTEX_POINT ( 'NONE', #11111 ) ;
#8083=DIRECTION ( 'NONE',  ( 0.000000000000000000, 0.000000000000000000, 1.000000000000000000 ) ) ;
#8097=CARTESIAN_POINT ( 'NONE',  ( 0.000000000000000000, -2.342598717236902051, 4.057500000000004547 ) ) ;
#8107=DIRECTION ( 'NONE',  ( 0.000000000000000000, 0.000000000000000000, -1.000000000000000000 ) ) ;
#8135=AXIS2_PLACEMENT_3D ( 'NONE', #8731, #10871, #8969 ) ;
#8169=DIRECTION ( 'NONE',  ( -1.000000000000000000, -0.000000000000000000, -0.000000000000000000 ) ) ;
#8176=TOROIDAL_SURFACE ( 'NONE', #4526, 6.500000000000000888, 1.500000000000000000 ) ;
#8202=EDGE_CURVE ( 'NONE', #4145, #9642, #5739, .T. ) ;
#8212=PLANE ( 'NONE',  #10936 ) ;
#8229=CARTESIAN_POINT ( 'NONE',  ( -31.74999999999995737, 0.000000000000000000, 0.000000000000000000 ) ) ;
#8280=CARTESIAN_POINT ( 'NONE',  ( 10.00000000000000000, 6.613092715395708453E-16, 5.400000000000001243 ) ) ;
#8312=CARTESIAN_POINT ( 'NONE',  ( 5.000000000000000000, 4.685197434473814759, -5.637851296924623057E-15 ) ) ;
#8353=FACE_OUTER_BOUND ( 'NONE', #1491, .T. ) ;
#8354=CARTESIAN_POINT ( 'NONE',  ( 5.000000000000000000, -4.685197434473812983, 6.938893903907228378E-15 ) ) ;
#8371=LINE ( 'NONE', #1582, #9212 ) ;
#8390=DIRECTION ( 'NONE',  ( -1.000000000000000000, -0.000000000000000000, -0.000000000000000000 ) ) ;
#8402=AXIS2_PLACEMENT_3D ( 'NONE', #2703, #2892, #10498 ) ;
#8414=DIRECTION ( 'NONE',  ( 0.000000000000000000, 0.000000000000000000, -1.000000000000000000 ) ) ;
#8454=DIRECTION ( 'NONE',  ( 0.000000000000000000, 0.000000000000000000, 1.000000000000000000 ) ) ;
#8464=CARTESIAN_POINT ( 'NONE',  ( 5.000000000000000000, 2.342598717236912265, 4.057499999999998330 ) ) ;
#8477=CARTESIAN_POINT ( 'NONE',  ( -31.74999999999995737, 0.000000000000000000, 5.000000000000000888 ) ) ;
#8486=ORIENTED_EDGE ( 'NONE', *, *, #868, .T. ) ;
#8491=AXIS2_PLACEMENT_3D ( 'NONE', #2192, #4986, #2889 ) ;
#8516=DIRECTION ( 'NONE',  ( -1.000000000000000000, -0.000000000000000000, -0.000000000000000000 ) ) ;
#8532=EDGE_CURVE ( 'NONE', #9642, #12368, #2529, .T. ) ;
#8552=CARTESIAN_POINT ( 'NONE',  ( 5.000000000000000000, 4.969004387540385421E-16, -4.057500000000000107 ) ) ;
#8554=CARTESIAN_POINT ( 'NONE',  ( 0.000000000000000000, -4.685197434473812983, 6.938893903907228378E-15 ) ) ;
#8557=DIRECTION ( 'NONE',  ( 0.000000000000000000, 0.000000000000000000, -1.000000000000000000 ) ) ;
#8589=CARTESIAN_POINT ( 'NONE',  ( 0.000000000000000000, 8.878689293818310074E-16, -6.500000000000000888 ) ) ;
#8612=AXIS2_PLACEMENT_3D ( 'NONE', #10369, #7648, #3646 ) ;
#8640=CARTESIAN_POINT ( 'NONE',  ( 5.000000000000000000, 4.685197434473814759, -5.637851296924623057E-15 ) ) ;
#8646=MECHANICAL_DESIGN_GEOMETRIC_PRESENTATION_REPRESENTATION('',(#9065),#10466);
#8651=EDGE_LOOP ( 'NONE', ( #2293, #6193, #767, #4642 ) ) ;
#8653=ORIENTED_EDGE ( 'NONE', *, *, #4424, .F. ) ;
#8656=AXIS2_PLACEMENT_3D ( 'NONE', #8640, #5548, #718 ) ;
#8660=PLANE ( 'NONE',  #6182 ) ;
#8674=CIRCLE ( 'NONE', #2593, 0.4000000000000001887 ) ;
#8681=DIRECTION ( 'NONE',  ( 1.000000000000000000, 0.000000000000000000, 0.000000000000000000 ) ) ;
#8683=DIRECTION ( 'NONE',  ( -0.5000000000000034417, 0.000000000000000000, 0.8660254037844367092 ) ) ;
#8717=CONICAL_SURFACE ( 'NONE', #11968, 4.057500000000000107, 1.047197551196593857 ) ;
#8719=CARTESIAN_POINT ( 'NONE',  ( 89.17200000000001125, 0.000000000000000000, 0.000000000000000000 ) ) ;
#8731=CARTESIAN_POINT ( 'NONE',  ( 10.40000000000000036, 0.000000000000000000, 0.000000000000000000 ) ) ;
#8774=ORIENTED_EDGE ( 'NONE', *, *, #8202, .F. ) ;
#8786=LINE ( 'NONE', #11769, #9706 ) ;
#8796=EDGE_LOOP ( 'NONE', ( #9927, #5352, #3020, #4125 ) ) ;
#8799=CARTESIAN_POINT ( 'NONE',  ( 5.000000000000000000, -2.342598717236902051, 4.057500000000004547 ) ) ;
#8804=DIRECTION ( 'NONE',  ( 0.000000000000000000, 0.000000000000000000, 1.000000000000000000 ) ) ;
#8815=CARTESIAN_POINT ( 'NONE',  ( 5.000000000000000000, -4.506943796211478080E-15, -4.057500000000000107 ) ) ;
#8828=EDGE_CURVE ( 'NONE', #10247, #1426, #11703, .T. ) ;
#8856=AXIS2_PLACEMENT_3D ( 'NONE', #9186, #11912, #8107 ) ;
#8884=AXIS2_PLACEMENT_3D ( 'NONE', #1439, #10129, #4350 ) ;
#8887=ORIENTED_EDGE ( 'NONE', *, *, #9449, .F. ) ;
#8928=EDGE_CURVE ( 'NONE', #6723, #12336, #1379, .T. ) ;
#8947=EDGE_CURVE ( 'NONE', #9642, #4145, #7242, .T. ) ;
#8954=CARTESIAN_POINT ( 'NONE',  ( 5.000000000000000000, 4.685197434473814759, -5.637851296924623057E-15 ) ) ;
#8969=DIRECTION ( 'NONE',  ( 0.000000000000000000, 0.000000000000000000, -1.000000000000000000 ) ) ;
#8971=EDGE_CURVE ( 'NONE', #2108, #12320, #9280, .T. ) ;
#8998=CARTESIAN_POINT ( 'NONE',  ( 1.500000000000001332, 0.000000000000000000, 0.000000000000000000 ) ) ;
#9016=ORIENTED_EDGE ( 'NONE', *, *, #930, .F. ) ;
#9021=AXIS2_PLACEMENT_3D ( 'NONE', #11433, #2744, #207 ) ;
#9059=CARTESIAN_POINT ( 'NONE',  ( 89.17200000000001125, 6.123233995736768255E-16, -5.000000000000001776 ) ) ;
#9065=STYLED_ITEM('',(#12591),#10428);
#9072=AXIS2_PLACEMENT_3D ( 'NONE', #6242, #1485, #535 ) ;
#9080=ORIENTED_EDGE ( 'NONE', *, *, #6506, .T. ) ;
#9130=ORIENTED_EDGE ( 'NONE', *, *, #11106, .T. ) ;
#9133=AXIS2_PLACEMENT_3D ( 'NONE', #2646, #3530, #7467 ) ;
#9146=PRODUCT_DEFINITION_SHAPE ( 'NONE', 'NONE',  #771 ) ;
#9157=ADVANCED_FACE ( 'NONE', ( #7504 ), #10473, .F. ) ;
#9171=EDGE_CURVE ( 'NONE', #6828, #1723, #5825, .T. ) ;
#9186=CARTESIAN_POINT ( 'NONE',  ( 10.00000000000000000, 0.000000000000000000, 0.000000000000000000 ) ) ;
#9188=DIRECTION ( 'NONE',  ( 0.000000000000000000, 0.4999999999999987232, -0.8660254037844392627 ) ) ;
#9192=AXIS2_PLACEMENT_3D ( 'NONE', #9437, #12351, #3650 ) ;
#9212=VECTOR ( 'NONE', #2591, 1000.000000000000114 ) ;
#9225=DIRECTION ( 'NONE',  ( 0.000000000000000000, 0.000000000000000000, -1.000000000000000000 ) ) ;
#9227=CARTESIAN_POINT ( 'NONE',  ( 5.000000000000000000, 2.342598717236900718, -4.057500000000001883 ) ) ;
#9228=DIRECTION ( 'NONE',  ( 0.000000000000000000, 0.000000000000000000, -1.000000000000000000 ) ) ;
#9235=ADVANCED_FACE ( 'NONE', ( #1607, #10537 ), #9478, .T. ) ;
#9269=PLANE ( 'NONE',  #6073 ) ;
#9280=CIRCLE ( 'NONE', #9072, 6.500000000000000888 ) ;
#9287=FACE_OUTER_BOUND ( 'NONE', #5832, .T. ) ;
#9290=VECTOR ( 'NONE', #2560, 1000.000000000000000 ) ;
#9349=EDGE_LOOP ( 'NONE', ( #1497, #3728, #12156, #9819 ) ) ;
#9372=DIRECTION ( 'NONE',  ( -1.000000000000000000, -0.000000000000000000, -0.000000000000000000 ) ) ;
#9381=DIRECTION ( 'NONE',  ( -1.000000000000000000, -0.000000000000000000, -0.000000000000000000 ) ) ;
#9427=ORIENTED_EDGE ( 'NONE', *, *, #4278, .F. ) ;
#9433=DIRECTION ( 'NONE',  ( -1.000000000000000000, -0.000000000000000000, -0.000000000000000000 ) ) ;
#9437=CARTESIAN_POINT ( 'NONE',  ( 10.40000000000000036, 0.000000000000000000, 0.000000000000000000 ) ) ;
#9449=EDGE_CURVE ( 'NONE', #6737, #2324, #6513, .T. ) ;
#9456=ORIENTED_EDGE ( 'NONE', *, *, #3507, .T. ) ;
#9478=PLANE ( 'NONE',  #7031 ) ;
#9572=DIRECTION ( 'NONE',  ( -1.000000000000000000, -0.000000000000000000, -0.000000000000000000 ) ) ;
#9582=TOROIDAL_SURFACE ( 'NONE', #10785, 5.400000000000001243, 0.4000000000000000222 ) ;
#9594=AXIS2_PLACEMENT_3D ( 'NONE', #5384, #5509, #1572 ) ;
#9620=PLANE ( 'NONE',  #112 ) ;
#9633=CIRCLE ( 'NONE', #12268, 4.057500000000000107 ) ;
#9642=VERTEX_POINT ( 'NONE', #9059 ) ;
#9670=DIRECTION ( 'NONE',  ( 0.000000000000000000, 0.8660254037844379305, -0.5000000000000014433 ) ) ;
#9677=VECTOR ( 'NONE', #7959, 1000.000000000000000 ) ;
#9680=LINE ( 'NONE', #988, #5561 ) ;
#9706=VECTOR ( 'NONE', #11647, 1000.000000000000000 ) ;
#9716=ORIENTED_EDGE ( 'NONE', *, *, #145, .T. ) ;
#9717=EDGE_CURVE ( 'NONE', #667, #4807, #2165, .T. ) ;
#9819=ORIENTED_EDGE ( 'NONE', *, *, #4212, .F. ) ;
#9821=DIRECTION ( 'NONE',  ( -1.000000000000000000, -0.000000000000000000, -0.000000000000000000 ) ) ;
#9832=DIRECTION ( 'NONE',  ( -0.7071067811865386910, 8.659560562355043792E-17, -0.7071067811865564545 ) ) ;
#9856=ADVANCED_FACE ( 'NONE', ( #115 ), #3086, .T. ) ;
#9865=EDGE_LOOP ( 'NONE', ( #2321, #12447, #9130, #3744 ) ) ;
#9867=CARTESIAN_POINT ( 'NONE',  ( 5.000000000000000000, -2.342598717236902051, 4.057500000000004547 ) ) ;
#9891=DIRECTION ( 'NONE',  ( 0.000000000000000000, 0.000000000000000000, -1.000000000000000000 ) ) ;
#9927=ORIENTED_EDGE ( 'NONE', *, *, #5383, .F. ) ;
#9969=VERTEX_POINT ( 'NONE', #5264 ) ;
#9972=ORIENTED_EDGE ( 'NONE', *, *, #10107, .T. ) ;
#10000=ORIENTED_EDGE ( 'NONE', *, *, #8828, .F. ) ;
#10012=PLANE ( 'NONE',  #2402 ) ;
#10047=CIRCLE ( 'NONE', #3948, 4.171999999999999709 ) ;
#10052=ORIENTED_EDGE ( 'NONE', *, *, #4424, .T. ) ;
#10074=DIRECTION ( 'NONE',  ( 1.000000000000000000, 0.000000000000000000, 0.000000000000000000 ) ) ;
#10107=EDGE_CURVE ( 'NONE', #7779, #6176, #685, .T. ) ;
#10113=AXIS2_PLACEMENT_3D ( 'NONE', #5949, #2010, #4103 ) ;
#10129=DIRECTION ( 'NONE',  ( -0.000000000000000000, 1.295896757998781572E-15, 1.000000000000000000 ) ) ;
#10246=LINE ( 'NONE', #5310, #11333 ) ;
#10247=VERTEX_POINT ( 'NONE', #8799 ) ;
#10251=DIRECTION ( 'NONE',  ( 0.000000000000000000, 0.4999999999999989453, -0.8660254037844391517 ) ) ;
#10255=PLANE ( 'NONE',  #2349 ) ;
#10278=CARTESIAN_POINT ( 'NONE',  ( 5.000000000000000000, 2.342598717236900718, -4.057500000000001883 ) ) ;
#10350=DIRECTION ( 'NONE',  ( 0.000000000000000000, 0.000000000000000000, 1.000000000000000000 ) ) ;
#10369=CARTESIAN_POINT ( 'NONE',  ( 1.500000000000001332, 0.000000000000000000, 0.000000000000000000 ) ) ;
#10390=FACE_OUTER_BOUND ( 'NONE', #7532, .T. ) ;
#10391=EDGE_CURVE ( 'NONE', #4807, #6993, #5010, .T. ) ;
#10425=ORIENTED_EDGE ( 'NONE', *, *, #8947, .F. ) ;
#10427=VECTOR ( 'NONE', #12468, 1000.000000000000000 ) ;
#10428=MANIFOLD_SOLID_BREP ( 'Hex', #798 ) ;
#10449=DIRECTION ( 'NONE',  ( -0.7071067811865386910, 0.000000000000000000, 0.7071067811865564545 ) ) ;
#10466=( GEOMETRIC_REPRESENTATION_CONTEXT ( 3 ) GLOBAL_UNCERTAINTY_ASSIGNED_CONTEXT ( ( #2897 ) ) GLOBAL_UNIT_ASSIGNED_CONTEXT ( ( #431, #3467, #1447 ) ) REPRESENTATION_CONTEXT ( 'NONE', 'WORKASPACE' ) );
#10468=EDGE_CURVE ( 'NONE', #8006, #2800, #6798, .T. ) ;
#10469=FACE_OUTER_BOUND ( 'NONE', #9865, .T. ) ;
#10473=PLANE ( 'NONE',  #8656 ) ;
#10498=DIRECTION ( 'NONE',  ( 0.000000000000000000, 0.000000000000000000, 1.000000000000000000 ) ) ;
#10523=EDGE_CURVE ( 'NONE', #10579, #11516, #7755, .T. ) ;
#10537=FACE_OUTER_BOUND ( 'NONE', #4062, .T. ) ;
#10573=LINE ( 'NONE', #8554, #11450 ) ;
#10579=VERTEX_POINT ( 'NONE', #10726 ) ;
#10593=ORIENTED_EDGE ( 'NONE', *, *, #5340, .T. ) ;
#10619=ORIENTED_EDGE ( 'NONE', *, *, #12308, .F. ) ;
#10685=CARTESIAN_POINT ( 'NONE',  ( 1.500000000000001332, 7.960204194457796463E-16, -6.500000000000000888 ) ) ;
#10688=DIRECTION ( 'NONE',  ( 0.000000000000000000, 1.000000000000000000, -1.110768649713241713E-15 ) ) ;
#10693=VECTOR ( 'NONE', #9832, 999.9999999999998863 ) ;
#10711=EDGE_CURVE ( 'NONE', #11516, #2324, #10573, .T. ) ;
#10726=CARTESIAN_POINT ( 'NONE',  ( 5.000000000000000000, -4.685197434473812983, 6.938893903907228378E-15 ) ) ;
#10753=EDGE_CURVE ( 'NONE', #12336, #6828, #9633, .T. ) ;
#10780=EDGE_LOOP ( 'NONE', ( #11618, #7700 ) ) ;
#10784=LINE ( 'NONE', #208, #4168 ) ;
#10785=AXIS2_PLACEMENT_3D ( 'NONE', #6041, #7881, #147 ) ;
#10796=VECTOR ( 'NONE', #1015, 1000.000000000000114 ) ;
#10810=ORIENTED_EDGE ( 'NONE', *, *, #4038, .F. ) ;
#10833=ADVANCED_FACE ( 'NONE', ( #2138 ), #12163, .T. ) ;
#10871=DIRECTION ( 'NONE',  ( 1.000000000000000000, 0.000000000000000000, 0.000000000000000000 ) ) ;
#10875=DIRECTION ( 'NONE',  ( -1.000000000000000000, -0.000000000000000000, -0.000000000000000000 ) ) ;
#10886=DIRECTION ( 'NONE',  ( -0.000000000000000000, 1.000000000000000000, 1.224646799147353207E-16 ) ) ;
#10910=AXIS2_PLACEMENT_3D ( 'NONE', #119, #5001, #3977 ) ;
#10936=AXIS2_PLACEMENT_3D ( 'NONE', #12142, #12081, #9228 ) ;
#10947=DIRECTION ( 'NONE',  ( 0.000000000000000000, -1.000000000000000000, 1.110768649713241713E-15 ) ) ;
#10958=EDGE_CURVE ( 'NONE', #5355, #2550, #6787, .T. ) ;
#10998=CARTESIAN_POINT ( 'NONE',  ( 5.000000000000000000, 4.685197434473814759, -5.637851296924623057E-15 ) ) ;
#11013=ADVANCED_FACE ( 'NONE', ( #3770 ), #9620, .F. ) ;
#11027=EDGE_CURVE ( 'NONE', #3844, #12462, #11247, .T. ) ;
#11031=ADVANCED_FACE ( 'NONE', ( #7588 ), #1924, .T. ) ;
#11049=APPLICATION_CONTEXT ( 'automotive_design' ) ;
#11074=ORIENTED_EDGE ( 'NONE', *, *, #868, .F. ) ;
#11080=DIRECTION ( 'NONE',  ( 0.000000000000000000, -0.5000000000000014433, -0.8660254037844379305 ) ) ;
#11092=VECTOR ( 'NONE', #7348, 1000.000000000000000 ) ;
#11101=EDGE_CURVE ( 'NONE', #5431, #169, #10047, .T. ) ;
#11106=EDGE_CURVE ( 'NONE', #4145, #667, #4728, .T. ) ;
#11111=CARTESIAN_POINT ( 'NONE',  ( 5.000000000000000000, 2.342598717236900718, -4.057500000000001883 ) ) ;
#11120=VECTOR ( 'NONE', #9188, 1000.000000000000227 ) ;
#11130=DIRECTION ( 'NONE',  ( -1.000000000000000000, -0.000000000000000000, -0.000000000000000000 ) ) ;
#11147=ADVANCED_FACE ( 'NONE', ( #927 ), #8660, .F. ) ;
#11193=LINE ( 'NONE', #8097, #3210 ) ;
#11242=EDGE_CURVE ( 'NONE', #12320, #2108, #6564, .T. ) ;
#11247=CIRCLE ( 'NONE', #2130, 8.000000000000000000 ) ;
#11254=CIRCLE ( 'NONE', #5990, 5.000000000000000888 ) ;
#11256=FACE_OUTER_BOUND ( 'NONE', #5088, .T. ) ;
#11259=CARTESIAN_POINT ( 'NONE',  ( 5.000000000000000000, 3.513898075855364400, 2.028749999999996945 ) ) ;
#11276=AXIS2_PLACEMENT_3D ( 'NONE', #11780, #9821, #4998 ) ;
#11283=CARTESIAN_POINT ( 'NONE',  ( 5.000000000000000000, -2.342598717236902051, 4.057500000000004547 ) ) ;
#11292=DIRECTION ( 'NONE',  ( 0.000000000000000000, -1.000000000000000000, 0.000000000000000000 ) ) ;
#11323=ORIENTED_EDGE ( 'NONE', *, *, #10523, .F. ) ;
#11333=VECTOR ( 'NONE', #4534, 1000.000000000000000 ) ;
#11342=ORIENTED_EDGE ( 'NONE', *, *, #6815, .T. ) ;
#11370=DIRECTION ( 'NONE',  ( -1.000000000000000000, -0.000000000000000000, -0.000000000000000000 ) ) ;
#11400=ORIENTED_EDGE ( 'NONE', *, *, #11242, .T. ) ;
#11414=ADVANCED_BREP_SHAPE_REPRESENTATION ( '', ( #10428, #9021 ), #6962 ) ;
#11433=CARTESIAN_POINT ( 'NONE',  ( 0.000000000000000000, 0.000000000000000000, 0.000000000000000000 ) ) ;
#11450=VECTOR ( 'NONE', #12421, 1000.000000000000227 ) ;
#11453=VECTOR ( 'NONE', #10449, 999.9999999999998863 ) ;
#11454=CARTESIAN_POINT ( 'NONE',  ( 10.00000000000000178, 0.000000000000000000, 0.000000000000000000 ) ) ;
#11462=ORIENTED_EDGE ( 'NONE', *, *, #11101, .T. ) ;
#11477=AXIS2_PLACEMENT_3D ( 'NONE', #11911, #4099, #4234 ) ;
#11504=ORIENTED_EDGE ( 'NONE', *, *, #12481, .T. ) ;
#11516=VERTEX_POINT ( 'NONE', #5611 ) ;
#11549=EDGE_LOOP ( 'NONE', ( #7956, #6942, #5497 ) ) ;
#11562=DIRECTION ( 'NONE',  ( -1.000000000000000000, -0.000000000000000000, -0.000000000000000000 ) ) ;
#11580=DIRECTION ( 'NONE',  ( 0.000000000000000000, 0.000000000000000000, -1.000000000000000000 ) ) ;
#11615=FACE_OUTER_BOUND ( 'NONE', #4407, .T. ) ;
#11618=ORIENTED_EDGE ( 'NONE', *, *, #5454, .T. ) ;
#11647=DIRECTION ( 'NONE',  ( -1.000000000000000000, -0.000000000000000000, -0.000000000000000000 ) ) ;
#11694=FACE_OUTER_BOUND ( 'NONE', #1511, .T. ) ;
#11700=ORIENTED_EDGE ( 'NONE', *, *, #7126, .T. ) ;
#11703=LINE ( 'NONE', #9867, #9677 ) ;
#11716=EDGE_CURVE ( 'NONE', #12336, #10579, #8371, .T. ) ;
#11764=CARTESIAN_POINT ( 'NONE',  ( 5.000000000000000000, 0.000000000000000000, 0.000000000000000000 ) ) ;
#11769=CARTESIAN_POINT ( 'NONE',  ( -31.74999999999995737, 0.000000000000000000, 8.000000000000000000 ) ) ;
#11772=AXIS2_PLACEMENT_3D ( 'NONE', #2614, #11370, #8454 ) ;
#11780=CARTESIAN_POINT ( 'NONE',  ( -31.74999999999995737, 0.000000000000000000, 0.000000000000000000 ) ) ;
#11787=CARTESIAN_POINT ( 'NONE',  ( 10.40000000000000036, 0.000000000000000000, 0.000000000000000000 ) ) ;
#11850=CARTESIAN_POINT ( 'NONE',  ( 90.00000000000000000, 0.000000000000000000, 4.171999999999999709 ) ) ;
#11903=LINE ( 'NONE', #4403, #4015 ) ;
#11906=VERTEX_POINT ( 'NONE', #12365 ) ;
#11908=ORIENTED_EDGE ( 'NONE', *, *, #4882, .T. ) ;
#11911=CARTESIAN_POINT ( 'NONE',  ( 10.40000000000000036, 6.613092715395708453E-16, 5.400000000000001243 ) ) ;
#11912=DIRECTION ( 'NONE',  ( -1.000000000000000000, -0.000000000000000000, -0.000000000000000000 ) ) ;
#11968=AXIS2_PLACEMENT_3D ( 'NONE', #6788, #1090, #2092 ) ;
#11975=AXIS2_PLACEMENT_3D ( 'NONE', #8954, #12061, #6344 ) ;
#11981=CARTESIAN_POINT ( 'NONE',  ( 5.000000000000000000, -3.513898075855362180, -2.028749999999995168 ) ) ;
#12023=CIRCLE ( 'NONE', #3916, 4.171999999999999709 ) ;
#12037=LINE ( 'NONE', #3339, #2510 ) ;
#12045=AXIS2_PLACEMENT_3D ( 'NONE', #539, #11130, #5238 ) ;
#12051=CARTESIAN_POINT ( 'NONE',  ( 5.000000000000000000, -2.342598717236911821, -4.057499999999996554 ) ) ;
#12056=DIRECTION ( 'NONE',  ( 0.000000000000000000, 1.000000000000000000, -1.295896757998781374E-15 ) ) ;
#12061=DIRECTION ( 'NONE',  ( 1.000000000000000000, 0.000000000000000000, 0.000000000000000000 ) ) ;
#12063=CARTESIAN_POINT ( 'NONE',  ( 5.000000000000000000, 0.000000000000000000, 0.000000000000000000 ) ) ;
#12066=( LENGTH_UNIT ( ) NAMED_UNIT ( * ) SI_UNIT ( .MILLI., .METRE. ) );
#12076=ORIENTED_EDGE ( 'NONE', *, *, #8202, .T. ) ;
#12081=DIRECTION ( 'NONE',  ( 1.000000000000000000, 0.000000000000000000, 0.000000000000000000 ) ) ;
#12095=LINE ( 'NONE', #6440, #4643 ) ;
#12100=CARTESIAN_POINT ( 'NONE',  ( 5.000000000000000000, -2.342598717236902051, 4.057500000000004547 ) ) ;
#12142=CARTESIAN_POINT ( 'NONE',  ( 10.00000000000000000, 8.000000000000000000, 0.000000000000000000 ) ) ;
#12156=ORIENTED_EDGE ( 'NONE', *, *, #5454, .F. ) ;
#12160=DIRECTION ( 'NONE',  ( 0.000000000000000000, 0.000000000000000000, 1.000000000000000000 ) ) ;
#12163=PLANE ( 'NONE',  #709 ) ;
#12165=AXIS2_PLACEMENT_3D ( 'NONE', #3743, #8390, #6538 ) ;
#12171=VECTOR ( 'NONE', #8683, 999.9999999999998863 ) ;
#12184=CIRCLE ( 'NONE', #6701, 4.057500000000000107 ) ;
#12186=ORIENTED_EDGE ( 'NONE', *, *, #5900, .T. ) ;
#12221=DIRECTION ( 'NONE',  ( 0.000000000000000000, 0.8660254037844380415, -0.5000000000000009992 ) ) ;
#12222=ADVANCED_FACE ( 'NONE', ( #5566 ), #8004, .T. ) ;
#12225=DIRECTION ( 'NONE',  ( -1.000000000000000000, -0.000000000000000000, -0.000000000000000000 ) ) ;
#12243=ORIENTED_EDGE ( 'NONE', *, *, #4750, .F. ) ;
#12260=ORIENTED_EDGE ( 'NONE', *, *, #2341, .T. ) ;
#12268=AXIS2_PLACEMENT_3D ( 'NONE', #6637, #6768, #3719 ) ;
#12282=EDGE_LOOP ( 'NONE', ( #3259, #10000, #5213, #351, #3069 ) ) ;
#12308=EDGE_CURVE ( 'NONE', #6176, #6737, #738, .T. ) ;
#12317=ORIENTED_EDGE ( 'NONE', *, *, #3157, .T. ) ;
#12320=VERTEX_POINT ( 'NONE', #7375 ) ;
#12336=VERTEX_POINT ( 'NONE', #7911 ) ;
#12351=DIRECTION ( 'NONE',  ( 1.000000000000000000, 0.000000000000000000, 0.000000000000000000 ) ) ;
#12363=CARTESIAN_POINT ( 'NONE',  ( 1.500000000000001332, 0.000000000000000000, 8.000000000000000000 ) ) ;
#12365=CARTESIAN_POINT ( 'NONE',  ( 0.000000000000000000, 2.342598717236912265, 4.057499999999998330 ) ) ;
#12368=VERTEX_POINT ( 'NONE', #4394 ) ;
#12371=LINE ( 'NONE', #2783, #7258 ) ;
#12421=DIRECTION ( 'NONE',  ( 0.000000000000000000, 0.4999999999999987232, -0.8660254037844392627 ) ) ;
#12447=ORIENTED_EDGE ( 'NONE', *, *, #8947, .T. ) ;
#12453=DIRECTION ( 'NONE',  ( -1.000000000000000000, -0.000000000000000000, -0.000000000000000000 ) ) ;
#12462=VERTEX_POINT ( 'NONE', #6074 ) ;
#12468=DIRECTION ( 'NONE',  ( -1.000000000000000000, -0.000000000000000000, -0.000000000000000000 ) ) ;
#12481=EDGE_CURVE ( 'NONE', #1426, #11516, #3149, .T. ) ;
#12530=CARTESIAN_POINT ( 'NONE',  ( 5.000000000000000000, 4.685197434473814759, -5.637851296924623057E-15 ) ) ;
#12536=ORIENTED_EDGE ( 'NONE', *, *, #11106, .F. ) ;
#12585=COLOUR_RGB('Black',0.12,0.14,0.17);
#12586=FILL_AREA_STYLE_COLOUR('',#12585);
#12587=FILL_AREA_STYLE('',(#12586));
#12588=SURFACE_STYLE_FILL_AREA(#12587);
#12589=SURFACE_SIDE_STYLE('',(#12588));
#12590=SURFACE_STYLE_USAGE(.BOTH.,#12589);
#12591=PRESENTATION_STYLE_ASSIGNMENT((#12590));
ENDSEC;
END-ISO-10303-21;
